ISO-10303-21;
HEADER;
/* Generated by software containing ST-Developer
 * from STEP Tools, Inc. (www.steptools.com) 
 */

FILE_DESCRIPTION(
/* description */ ('Turntable on roller ring'),
/* implementation_level */ '2;1');

FILE_NAME(
/* name */ 'Roller bracket (3).step',
/* time_stamp */ '2026-10-28T03:23:59-07:00',
/* author */ (''),
/* organization */ (''),
/* preprocessor_version */ 'ST-DEVELOPER v20.2',
/* originating_system */ 'Autodesk Translation Framework v15.17.0.0',
/* authorisation */ '');

FILE_SCHEMA (('AUTOMOTIVE_DESIGN { 1 0 10303 214 3 1 1 }'));
ENDSEC;

DATA;
#10=MECHANICAL_DESIGN_GEOMETRIC_PRESENTATION_REPRESENTATION('',(#657),#16281);
#538=SHAPE_REPRESENTATION_RELATIONSHIP('SRR','None',#16558,#593);
#593=ADVANCED_BREP_SHAPE_REPRESENTATION('',(#727),#16252);
#657=STYLED_ITEM('',(#16911),#727);
#727=MANIFOLD_SOLID_BREP('Body1',#8400);
#933=FACE_BOUND('',#2274,.T.);
#934=FACE_BOUND('',#2276,.T.);
#935=FACE_BOUND('',#2281,.T.);
#936=FACE_BOUND('',#2283,.T.);
#937=FACE_BOUND('',#2289,.T.);
#938=FACE_BOUND('',#2290,.T.);
#939=FACE_BOUND('',#2291,.T.);
#940=FACE_BOUND('',#2292,.T.);
#941=FACE_BOUND('',#2293,.T.);
#942=FACE_BOUND('',#2294,.T.);
#943=FACE_BOUND('',#2296,.T.);
#944=FACE_BOUND('',#2297,.T.);
#945=FACE_BOUND('',#2298,.T.);
#946=FACE_BOUND('',#2299,.T.);
#1161=PLANE('',#9783);
#1162=PLANE('',#9784);
#1163=PLANE('',#9785);
#1164=PLANE('',#9786);
#1165=PLANE('',#9787);
#1166=PLANE('',#9788);
#1167=PLANE('',#9789);
#1168=PLANE('',#9790);
#1169=PLANE('',#9791);
#1170=PLANE('',#9792);
#1171=PLANE('',#9793);
#1172=PLANE('',#9794);
#1173=PLANE('',#9795);
#1174=PLANE('',#9796);
#1175=PLANE('',#9797);
#1176=PLANE('',#9798);
#1583=FACE_OUTER_BOUND('',#2264,.T.);
#1584=FACE_OUTER_BOUND('',#2265,.T.);
#1585=FACE_OUTER_BOUND('',#2266,.T.);
#1586=FACE_OUTER_BOUND('',#2267,.T.);
#1587=FACE_OUTER_BOUND('',#2268,.T.);
#1588=FACE_OUTER_BOUND('',#2269,.T.);
#1589=FACE_OUTER_BOUND('',#2270,.T.);
#1590=FACE_OUTER_BOUND('',#2271,.T.);
#1591=FACE_OUTER_BOUND('',#2272,.T.);
#1592=FACE_OUTER_BOUND('',#2273,.T.);
#1593=FACE_OUTER_BOUND('',#2275,.T.);
#1594=FACE_OUTER_BOUND('',#2277,.T.);
#1595=FACE_OUTER_BOUND('',#2278,.T.);
#1596=FACE_OUTER_BOUND('',#2279,.T.);
#1597=FACE_OUTER_BOUND('',#2280,.T.);
#1598=FACE_OUTER_BOUND('',#2282,.T.);
#1599=FACE_OUTER_BOUND('',#2284,.T.);
#1600=FACE_OUTER_BOUND('',#2285,.T.);
#1601=FACE_OUTER_BOUND('',#2286,.T.);
#1602=FACE_OUTER_BOUND('',#2287,.T.);
#1603=FACE_OUTER_BOUND('',#2288,.T.);
#1604=FACE_OUTER_BOUND('',#2295,.T.);
#2264=EDGE_LOOP('',(#7031,#7032,#7033,#7034));
#2265=EDGE_LOOP('',(#7035,#7036,#7037,#7038));
#2266=EDGE_LOOP('',(#7039,#7040,#7041,#7042));
#2267=EDGE_LOOP('',(#7043,#7044,#7045,#7046));
#2268=EDGE_LOOP('',(#7047,#7048,#7049,#7050));
#2269=EDGE_LOOP('',(#7051,#7052,#7053,#7054));
#2270=EDGE_LOOP('',(#7055,#7056,#7057,#7058));
#2271=EDGE_LOOP('',(#7059,#7060,#7061,#7062));
#2272=EDGE_LOOP('',(#7063,#7064,#7065,#7066));
#2273=EDGE_LOOP('',(#7067,#7068,#7069,#7070));
#2274=EDGE_LOOP('',(#7071));
#2275=EDGE_LOOP('',(#7072,#7073,#7074,#7075));
#2276=EDGE_LOOP('',(#7076));
#2277=EDGE_LOOP('',(#7077,#7078,#7079,#7080));
#2278=EDGE_LOOP('',(#7081,#7082,#7083,#7084));
#2279=EDGE_LOOP('',(#7085,#7086,#7087,#7088));
#2280=EDGE_LOOP('',(#7089,#7090,#7091,#7092));
#2281=EDGE_LOOP('',(#7093));
#2282=EDGE_LOOP('',(#7094,#7095,#7096,#7097));
#2283=EDGE_LOOP('',(#7098));
#2284=EDGE_LOOP('',(#7099,#7100,#7101,#7102));
#2285=EDGE_LOOP('',(#7103,#7104,#7105,#7106));
#2286=EDGE_LOOP('',(#7107,#7108,#7109,#7110));
#2287=EDGE_LOOP('',(#7111,#7112,#7113,#7114));
#2288=EDGE_LOOP('',(#7115,#7116,#7117,#7118));
#2289=EDGE_LOOP('',(#7119,#7120,#7121,#7122));
#2290=EDGE_LOOP('',(#7123,#7124,#7125,#7126));
#2291=EDGE_LOOP('',(#7127));
#2292=EDGE_LOOP('',(#7128));
#2293=EDGE_LOOP('',(#7129));
#2294=EDGE_LOOP('',(#7130));
#2295=EDGE_LOOP('',(#7131,#7132,#7133,#7134));
#2296=EDGE_LOOP('',(#7135));
#2297=EDGE_LOOP('',(#7136));
#2298=EDGE_LOOP('',(#7137));
#2299=EDGE_LOOP('',(#7138));
#2839=LINE('',#15000,#3322);
#2840=LINE('',#15006,#3323);
#2841=LINE('',#15012,#3324);
#2842=LINE('',#15018,#3325);
#2843=LINE('',#15024,#3326);
#2844=LINE('',#15030,#3327);
#2845=LINE('',#15035,#3328);
#2846=LINE('',#15037,#3329);
#2847=LINE('',#15039,#3330);
#2848=LINE('',#15040,#3331);
#2849=LINE('',#15044,#3332);
#2850=LINE('',#15046,#3333);
#2851=LINE('',#15048,#3334);
#2852=LINE('',#15049,#3335);
#2853=LINE('',#15051,#3336);
#2854=LINE('',#15052,#3337);
#2855=LINE('',#15054,#3338);
#2856=LINE('',#15056,#3339);
#2857=LINE('',#15060,#3340);
#2858=LINE('',#15062,#3341);
#2859=LINE('',#15064,#3342);
#2860=LINE('',#15065,#3343);
#2861=LINE('',#15069,#3344);
#2862=LINE('',#15071,#3345);
#2863=LINE('',#15073,#3346);
#2864=LINE('',#15074,#3347);
#2865=LINE('',#15076,#3348);
#2866=LINE('',#15077,#3349);
#2867=LINE('',#15079,#3350);
#2868=LINE('',#15081,#3351);
#2869=LINE('',#15085,#3352);
#2870=LINE('',#15087,#3353);
#2871=LINE('',#15089,#3354);
#2872=LINE('',#15090,#3355);
#2873=LINE('',#15093,#3356);
#2874=LINE('',#15095,#3357);
#2875=LINE('',#15096,#3358);
#2876=LINE('',#15099,#3359);
#2877=LINE('',#15101,#3360);
#2878=LINE('',#15102,#3361);
#2879=LINE('',#15104,#3362);
#2880=LINE('',#15105,#3363);
#3322=VECTOR('',#12000,0.275);
#3323=VECTOR('',#12007,0.275);
#3324=VECTOR('',#12014,0.275);
#3325=VECTOR('',#12021,0.275);
#3326=VECTOR('',#12028,0.5);
#3327=VECTOR('',#12035,0.5);
#3328=VECTOR('',#12040,1.);
#3329=VECTOR('',#12041,1.);
#3330=VECTOR('',#12042,1.);
#3331=VECTOR('',#12043,1.);
#3332=VECTOR('',#12046,1.);
#3333=VECTOR('',#12047,1.);
#3334=VECTOR('',#12048,1.);
#3335=VECTOR('',#12049,1.);
#3336=VECTOR('',#12052,1.);
#3337=VECTOR('',#12053,1.);
#3338=VECTOR('',#12056,1.);
#3339=VECTOR('',#12059,1.);
#3340=VECTOR('',#12062,1.);
#3341=VECTOR('',#12063,1.);
#3342=VECTOR('',#12064,1.);
#3343=VECTOR('',#12065,1.);
#3344=VECTOR('',#12068,1.);
#3345=VECTOR('',#12069,1.);
#3346=VECTOR('',#12070,1.);
#3347=VECTOR('',#12071,1.);
#3348=VECTOR('',#12074,1.);
#3349=VECTOR('',#12075,1.);
#3350=VECTOR('',#12078,1.);
#3351=VECTOR('',#12081,1.);
#3352=VECTOR('',#12084,1.);
#3353=VECTOR('',#12085,1.);
#3354=VECTOR('',#12086,1.);
#3355=VECTOR('',#12087,1.);
#3356=VECTOR('',#12090,1.);
#3357=VECTOR('',#12091,1.);
#3358=VECTOR('',#12092,1.);
#3359=VECTOR('',#12095,1.);
#3360=VECTOR('',#12096,1.);
#3361=VECTOR('',#12097,1.);
#3362=VECTOR('',#12100,1.);
#3363=VECTOR('',#12101,1.);
#3785=CIRCLE('',#9766,0.275);
#3786=CIRCLE('',#9767,0.275);
#3787=CIRCLE('',#9769,0.275);
#3788=CIRCLE('',#9770,0.275);
#3789=CIRCLE('',#9772,0.275);
#3790=CIRCLE('',#9773,0.275);
#3791=CIRCLE('',#9775,0.275);
#3792=CIRCLE('',#9776,0.275);
#3793=CIRCLE('',#9778,0.5);
#3794=CIRCLE('',#9779,0.5);
#3795=CIRCLE('',#9781,0.5);
#3796=CIRCLE('',#9782,0.5);
#4413=VERTEX_POINT('',#14997);
#4414=VERTEX_POINT('',#14999);
#4415=VERTEX_POINT('',#15003);
#4416=VERTEX_POINT('',#15005);
#4417=VERTEX_POINT('',#15009);
#4418=VERTEX_POINT('',#15011);
#4419=VERTEX_POINT('',#15015);
#4420=VERTEX_POINT('',#15017);
#4421=VERTEX_POINT('',#15021);
#4422=VERTEX_POINT('',#15023);
#4423=VERTEX_POINT('',#15027);
#4424=VERTEX_POINT('',#15029);
#4425=VERTEX_POINT('',#15033);
#4426=VERTEX_POINT('',#15034);
#4427=VERTEX_POINT('',#15036);
#4428=VERTEX_POINT('',#15038);
#4429=VERTEX_POINT('',#15042);
#4430=VERTEX_POINT('',#15043);
#4431=VERTEX_POINT('',#15045);
#4432=VERTEX_POINT('',#15047);
#4433=VERTEX_POINT('',#15058);
#4434=VERTEX_POINT('',#15059);
#4435=VERTEX_POINT('',#15061);
#4436=VERTEX_POINT('',#15063);
#4437=VERTEX_POINT('',#15067);
#4438=VERTEX_POINT('',#15068);
#4439=VERTEX_POINT('',#15070);
#4440=VERTEX_POINT('',#15072);
#4441=VERTEX_POINT('',#15083);
#4442=VERTEX_POINT('',#15084);
#4443=VERTEX_POINT('',#15086);
#4444=VERTEX_POINT('',#15088);
#4445=VERTEX_POINT('',#15092);
#4446=VERTEX_POINT('',#15094);
#4447=VERTEX_POINT('',#15098);
#4448=VERTEX_POINT('',#15100);
#5326=EDGE_CURVE('',#4413,#4413,#3785,.T.);
#5327=EDGE_CURVE('',#4413,#4414,#2839,.T.);
#5328=EDGE_CURVE('',#4414,#4414,#3786,.T.);
#5329=EDGE_CURVE('',#4415,#4415,#3787,.T.);
#5330=EDGE_CURVE('',#4415,#4416,#2840,.T.);
#5331=EDGE_CURVE('',#4416,#4416,#3788,.T.);
#5332=EDGE_CURVE('',#4417,#4417,#3789,.T.);
#5333=EDGE_CURVE('',#4417,#4418,#2841,.T.);
#5334=EDGE_CURVE('',#4418,#4418,#3790,.T.);
#5335=EDGE_CURVE('',#4419,#4419,#3791,.T.);
#5336=EDGE_CURVE('',#4419,#4420,#2842,.T.);
#5337=EDGE_CURVE('',#4420,#4420,#3792,.T.);
#5338=EDGE_CURVE('',#4421,#4421,#3793,.T.);
#5339=EDGE_CURVE('',#4421,#4422,#2843,.T.);
#5340=EDGE_CURVE('',#4422,#4422,#3794,.T.);
#5341=EDGE_CURVE('',#4423,#4423,#3795,.T.);
#5342=EDGE_CURVE('',#4423,#4424,#2844,.T.);
#5343=EDGE_CURVE('',#4424,#4424,#3796,.T.);
#5344=EDGE_CURVE('',#4425,#4426,#2845,.T.);
#5345=EDGE_CURVE('',#4425,#4427,#2846,.T.);
#5346=EDGE_CURVE('',#4428,#4427,#2847,.T.);
#5347=EDGE_CURVE('',#4426,#4428,#2848,.T.);
#5348=EDGE_CURVE('',#4429,#4430,#2849,.T.);
#5349=EDGE_CURVE('',#4431,#4429,#2850,.T.);
#5350=EDGE_CURVE('',#4432,#4431,#2851,.T.);
#5351=EDGE_CURVE('',#4430,#4432,#2852,.T.);
#5352=EDGE_CURVE('',#4430,#4425,#2853,.T.);
#5353=EDGE_CURVE('',#4427,#4432,#2854,.T.);
#5354=EDGE_CURVE('',#4428,#4431,#2855,.T.);
#5355=EDGE_CURVE('',#4429,#4426,#2856,.T.);
#5356=EDGE_CURVE('',#4433,#4434,#2857,.T.);
#5357=EDGE_CURVE('',#4433,#4435,#2858,.T.);
#5358=EDGE_CURVE('',#4436,#4435,#2859,.T.);
#5359=EDGE_CURVE('',#4434,#4436,#2860,.T.);
#5360=EDGE_CURVE('',#4437,#4438,#2861,.T.);
#5361=EDGE_CURVE('',#4439,#4437,#2862,.T.);
#5362=EDGE_CURVE('',#4440,#4439,#2863,.T.);
#5363=EDGE_CURVE('',#4438,#4440,#2864,.T.);
#5364=EDGE_CURVE('',#4438,#4433,#2865,.T.);
#5365=EDGE_CURVE('',#4435,#4440,#2866,.T.);
#5366=EDGE_CURVE('',#4436,#4439,#2867,.T.);
#5367=EDGE_CURVE('',#4437,#4434,#2868,.T.);
#5368=EDGE_CURVE('',#4441,#4442,#2869,.T.);
#5369=EDGE_CURVE('',#4442,#4443,#2870,.T.);
#5370=EDGE_CURVE('',#4444,#4443,#2871,.T.);
#5371=EDGE_CURVE('',#4441,#4444,#2872,.T.);
#5372=EDGE_CURVE('',#4445,#4441,#2873,.T.);
#5373=EDGE_CURVE('',#4446,#4444,#2874,.T.);
#5374=EDGE_CURVE('',#4445,#4446,#2875,.T.);
#5375=EDGE_CURVE('',#4447,#4445,#2876,.T.);
#5376=EDGE_CURVE('',#4448,#4446,#2877,.T.);
#5377=EDGE_CURVE('',#4447,#4448,#2878,.T.);
#5378=EDGE_CURVE('',#4442,#4447,#2879,.T.);
#5379=EDGE_CURVE('',#4443,#4448,#2880,.T.);
#7031=ORIENTED_EDGE('',*,*,#5326,.F.);
#7032=ORIENTED_EDGE('',*,*,#5327,.T.);
#7033=ORIENTED_EDGE('',*,*,#5328,.F.);
#7034=ORIENTED_EDGE('',*,*,#5327,.F.);
#7035=ORIENTED_EDGE('',*,*,#5329,.F.);
#7036=ORIENTED_EDGE('',*,*,#5330,.T.);
#7037=ORIENTED_EDGE('',*,*,#5331,.F.);
#7038=ORIENTED_EDGE('',*,*,#5330,.F.);
#7039=ORIENTED_EDGE('',*,*,#5332,.F.);
#7040=ORIENTED_EDGE('',*,*,#5333,.T.);
#7041=ORIENTED_EDGE('',*,*,#5334,.F.);
#7042=ORIENTED_EDGE('',*,*,#5333,.F.);
#7043=ORIENTED_EDGE('',*,*,#5335,.F.);
#7044=ORIENTED_EDGE('',*,*,#5336,.T.);
#7045=ORIENTED_EDGE('',*,*,#5337,.F.);
#7046=ORIENTED_EDGE('',*,*,#5336,.F.);
#7047=ORIENTED_EDGE('',*,*,#5338,.F.);
#7048=ORIENTED_EDGE('',*,*,#5339,.T.);
#7049=ORIENTED_EDGE('',*,*,#5340,.F.);
#7050=ORIENTED_EDGE('',*,*,#5339,.F.);
#7051=ORIENTED_EDGE('',*,*,#5341,.F.);
#7052=ORIENTED_EDGE('',*,*,#5342,.T.);
#7053=ORIENTED_EDGE('',*,*,#5343,.F.);
#7054=ORIENTED_EDGE('',*,*,#5342,.F.);
#7055=ORIENTED_EDGE('',*,*,#5344,.F.);
#7056=ORIENTED_EDGE('',*,*,#5345,.T.);
#7057=ORIENTED_EDGE('',*,*,#5346,.F.);
#7058=ORIENTED_EDGE('',*,*,#5347,.F.);
#7059=ORIENTED_EDGE('',*,*,#5348,.F.);
#7060=ORIENTED_EDGE('',*,*,#5349,.F.);
#7061=ORIENTED_EDGE('',*,*,#5350,.F.);
#7062=ORIENTED_EDGE('',*,*,#5351,.F.);
#7063=ORIENTED_EDGE('',*,*,#5352,.F.);
#7064=ORIENTED_EDGE('',*,*,#5351,.T.);
#7065=ORIENTED_EDGE('',*,*,#5353,.F.);
#7066=ORIENTED_EDGE('',*,*,#5345,.F.);
#7067=ORIENTED_EDGE('',*,*,#5353,.T.);
#7068=ORIENTED_EDGE('',*,*,#5350,.T.);
#7069=ORIENTED_EDGE('',*,*,#5354,.F.);
#7070=ORIENTED_EDGE('',*,*,#5346,.T.);
#7071=ORIENTED_EDGE('',*,*,#5343,.T.);
#7072=ORIENTED_EDGE('',*,*,#5352,.T.);
#7073=ORIENTED_EDGE('',*,*,#5344,.T.);
#7074=ORIENTED_EDGE('',*,*,#5355,.F.);
#7075=ORIENTED_EDGE('',*,*,#5348,.T.);
#7076=ORIENTED_EDGE('',*,*,#5341,.T.);
#7077=ORIENTED_EDGE('',*,*,#5356,.F.);
#7078=ORIENTED_EDGE('',*,*,#5357,.T.);
#7079=ORIENTED_EDGE('',*,*,#5358,.F.);
#7080=ORIENTED_EDGE('',*,*,#5359,.F.);
#7081=ORIENTED_EDGE('',*,*,#5360,.F.);
#7082=ORIENTED_EDGE('',*,*,#5361,.F.);
#7083=ORIENTED_EDGE('',*,*,#5362,.F.);
#7084=ORIENTED_EDGE('',*,*,#5363,.F.);
#7085=ORIENTED_EDGE('',*,*,#5364,.F.);
#7086=ORIENTED_EDGE('',*,*,#5363,.T.);
#7087=ORIENTED_EDGE('',*,*,#5365,.F.);
#7088=ORIENTED_EDGE('',*,*,#5357,.F.);
#7089=ORIENTED_EDGE('',*,*,#5365,.T.);
#7090=ORIENTED_EDGE('',*,*,#5362,.T.);
#7091=ORIENTED_EDGE('',*,*,#5366,.F.);
#7092=ORIENTED_EDGE('',*,*,#5358,.T.);
#7093=ORIENTED_EDGE('',*,*,#5340,.T.);
#7094=ORIENTED_EDGE('',*,*,#5364,.T.);
#7095=ORIENTED_EDGE('',*,*,#5356,.T.);
#7096=ORIENTED_EDGE('',*,*,#5367,.F.);
#7097=ORIENTED_EDGE('',*,*,#5360,.T.);
#7098=ORIENTED_EDGE('',*,*,#5338,.T.);
#7099=ORIENTED_EDGE('',*,*,#5368,.T.);
#7100=ORIENTED_EDGE('',*,*,#5369,.T.);
#7101=ORIENTED_EDGE('',*,*,#5370,.F.);
#7102=ORIENTED_EDGE('',*,*,#5371,.F.);
#7103=ORIENTED_EDGE('',*,*,#5372,.T.);
#7104=ORIENTED_EDGE('',*,*,#5371,.T.);
#7105=ORIENTED_EDGE('',*,*,#5373,.F.);
#7106=ORIENTED_EDGE('',*,*,#5374,.F.);
#7107=ORIENTED_EDGE('',*,*,#5375,.T.);
#7108=ORIENTED_EDGE('',*,*,#5374,.T.);
#7109=ORIENTED_EDGE('',*,*,#5376,.F.);
#7110=ORIENTED_EDGE('',*,*,#5377,.F.);
#7111=ORIENTED_EDGE('',*,*,#5378,.T.);
#7112=ORIENTED_EDGE('',*,*,#5377,.T.);
#7113=ORIENTED_EDGE('',*,*,#5379,.F.);
#7114=ORIENTED_EDGE('',*,*,#5369,.F.);
#7115=ORIENTED_EDGE('',*,*,#5379,.T.);
#7116=ORIENTED_EDGE('',*,*,#5376,.T.);
#7117=ORIENTED_EDGE('',*,*,#5373,.T.);
#7118=ORIENTED_EDGE('',*,*,#5370,.T.);
#7119=ORIENTED_EDGE('',*,*,#5361,.T.);
#7120=ORIENTED_EDGE('',*,*,#5367,.T.);
#7121=ORIENTED_EDGE('',*,*,#5359,.T.);
#7122=ORIENTED_EDGE('',*,*,#5366,.T.);
#7123=ORIENTED_EDGE('',*,*,#5349,.T.);
#7124=ORIENTED_EDGE('',*,*,#5355,.T.);
#7125=ORIENTED_EDGE('',*,*,#5347,.T.);
#7126=ORIENTED_EDGE('',*,*,#5354,.T.);
#7127=ORIENTED_EDGE('',*,*,#5337,.T.);
#7128=ORIENTED_EDGE('',*,*,#5334,.T.);
#7129=ORIENTED_EDGE('',*,*,#5331,.T.);
#7130=ORIENTED_EDGE('',*,*,#5328,.T.);
#7131=ORIENTED_EDGE('',*,*,#5378,.F.);
#7132=ORIENTED_EDGE('',*,*,#5368,.F.);
#7133=ORIENTED_EDGE('',*,*,#5372,.F.);
#7134=ORIENTED_EDGE('',*,*,#5375,.F.);
#7135=ORIENTED_EDGE('',*,*,#5326,.T.);
#7136=ORIENTED_EDGE('',*,*,#5329,.T.);
#7137=ORIENTED_EDGE('',*,*,#5332,.T.);
#7138=ORIENTED_EDGE('',*,*,#5335,.T.);
#7798=CYLINDRICAL_SURFACE('',#9765,0.275);
#7799=CYLINDRICAL_SURFACE('',#9768,0.275);
#7800=CYLINDRICAL_SURFACE('',#9771,0.275);
#7801=CYLINDRICAL_SURFACE('',#9774,0.275);
#7802=CYLINDRICAL_SURFACE('',#9777,0.5);
#7803=CYLINDRICAL_SURFACE('',#9780,0.5);
#8186=ADVANCED_FACE('',(#1583),#7798,.F.);
#8187=ADVANCED_FACE('',(#1584),#7799,.F.);
#8188=ADVANCED_FACE('',(#1585),#7800,.F.);
#8189=ADVANCED_FACE('',(#1586),#7801,.F.);
#8190=ADVANCED_FACE('',(#1587),#7802,.F.);
#8191=ADVANCED_FACE('',(#1588),#7803,.F.);
#8192=ADVANCED_FACE('',(#1589),#1161,.T.);
#8193=ADVANCED_FACE('',(#1590),#1162,.T.);
#8194=ADVANCED_FACE('',(#1591),#1163,.T.);
#8195=ADVANCED_FACE('',(#1592,#933),#1164,.T.);
#8196=ADVANCED_FACE('',(#1593,#934),#1165,.F.);
#8197=ADVANCED_FACE('',(#1594),#1166,.T.);
#8198=ADVANCED_FACE('',(#1595),#1167,.T.);
#8199=ADVANCED_FACE('',(#1596),#1168,.T.);
#8200=ADVANCED_FACE('',(#1597,#935),#1169,.T.);
#8201=ADVANCED_FACE('',(#1598,#936),#1170,.F.);
#8202=ADVANCED_FACE('',(#1599),#1171,.T.);
#8203=ADVANCED_FACE('',(#1600),#1172,.T.);
#8204=ADVANCED_FACE('',(#1601),#1173,.T.);
#8205=ADVANCED_FACE('',(#1602),#1174,.T.);
#8206=ADVANCED_FACE('',(#1603,#937,#938,#939,#940,#941,#942),#1175,.T.);
#8207=ADVANCED_FACE('',(#1604,#943,#944,#945,#946),#1176,.F.);
#8400=CLOSED_SHELL('',(#8186,#8187,#8188,#8189,#8190,#8191,#8192,#8193,
#8194,#8195,#8196,#8197,#8198,#8199,#8200,#8201,#8202,#8203,#8204,#8205,
#8206,#8207));
#9764=AXIS2_PLACEMENT_3D('',#14995,#11994,#11995);
#9765=AXIS2_PLACEMENT_3D('',#14996,#11996,#11997);
#9766=AXIS2_PLACEMENT_3D('',#14998,#11998,#11999);
#9767=AXIS2_PLACEMENT_3D('',#15001,#12001,#12002);
#9768=AXIS2_PLACEMENT_3D('',#15002,#12003,#12004);
#9769=AXIS2_PLACEMENT_3D('',#15004,#12005,#12006);
#9770=AXIS2_PLACEMENT_3D('',#15007,#12008,#12009);
#9771=AXIS2_PLACEMENT_3D('',#15008,#12010,#12011);
#9772=AXIS2_PLACEMENT_3D('',#15010,#12012,#12013);
#9773=AXIS2_PLACEMENT_3D('',#15013,#12015,#12016);
#9774=AXIS2_PLACEMENT_3D('',#15014,#12017,#12018);
#9775=AXIS2_PLACEMENT_3D('',#15016,#12019,#12020);
#9776=AXIS2_PLACEMENT_3D('',#15019,#12022,#12023);
#9777=AXIS2_PLACEMENT_3D('',#15020,#12024,#12025);
#9778=AXIS2_PLACEMENT_3D('',#15022,#12026,#12027);
#9779=AXIS2_PLACEMENT_3D('',#15025,#12029,#12030);
#9780=AXIS2_PLACEMENT_3D('',#15026,#12031,#12032);
#9781=AXIS2_PLACEMENT_3D('',#15028,#12033,#12034);
#9782=AXIS2_PLACEMENT_3D('',#15031,#12036,#12037);
#9783=AXIS2_PLACEMENT_3D('',#15032,#12038,#12039);
#9784=AXIS2_PLACEMENT_3D('',#15041,#12044,#12045);
#9785=AXIS2_PLACEMENT_3D('',#15050,#12050,#12051);
#9786=AXIS2_PLACEMENT_3D('',#15053,#12054,#12055);
#9787=AXIS2_PLACEMENT_3D('',#15055,#12057,#12058);
#9788=AXIS2_PLACEMENT_3D('',#15057,#12060,#12061);
#9789=AXIS2_PLACEMENT_3D('',#15066,#12066,#12067);
#9790=AXIS2_PLACEMENT_3D('',#15075,#12072,#12073);
#9791=AXIS2_PLACEMENT_3D('',#15078,#12076,#12077);
#9792=AXIS2_PLACEMENT_3D('',#15080,#12079,#12080);
#9793=AXIS2_PLACEMENT_3D('',#15082,#12082,#12083);
#9794=AXIS2_PLACEMENT_3D('',#15091,#12088,#12089);
#9795=AXIS2_PLACEMENT_3D('',#15097,#12093,#12094);
#9796=AXIS2_PLACEMENT_3D('',#15103,#12098,#12099);
#9797=AXIS2_PLACEMENT_3D('',#15106,#12102,#12103);
#9798=AXIS2_PLACEMENT_3D('',#15107,#12104,#12105);
#11994=DIRECTION('axis',(0.,0.,1.));
#11995=DIRECTION('refdir',(1.,0.,0.));
#11996=DIRECTION('center_axis',(0.,0.,1.));
#11997=DIRECTION('ref_axis',(1.,0.,0.));
#11998=DIRECTION('center_axis',(0.,0.,1.));
#11999=DIRECTION('ref_axis',(1.,0.,0.));
#12000=DIRECTION('',(0.,0.,1.));
#12001=DIRECTION('center_axis',(0.,0.,-1.));
#12002=DIRECTION('ref_axis',(1.,0.,0.));
#12003=DIRECTION('center_axis',(0.,0.,1.));
#12004=DIRECTION('ref_axis',(1.,0.,0.));
#12005=DIRECTION('center_axis',(0.,0.,1.));
#12006=DIRECTION('ref_axis',(1.,0.,0.));
#12007=DIRECTION('',(0.,0.,1.));
#12008=DIRECTION('center_axis',(0.,0.,-1.));
#12009=DIRECTION('ref_axis',(1.,0.,0.));
#12010=DIRECTION('center_axis',(0.,0.,1.));
#12011=DIRECTION('ref_axis',(1.,0.,0.));
#12012=DIRECTION('center_axis',(0.,0.,1.));
#12013=DIRECTION('ref_axis',(1.,0.,0.));
#12014=DIRECTION('',(0.,0.,1.));
#12015=DIRECTION('center_axis',(0.,0.,-1.));
#12016=DIRECTION('ref_axis',(1.,0.,0.));
#12017=DIRECTION('center_axis',(0.,0.,1.));
#12018=DIRECTION('ref_axis',(1.,0.,0.));
#12019=DIRECTION('center_axis',(0.,0.,1.));
#12020=DIRECTION('ref_axis',(1.,0.,0.));
#12021=DIRECTION('',(0.,0.,1.));
#12022=DIRECTION('center_axis',(0.,0.,-1.));
#12023=DIRECTION('ref_axis',(1.,0.,0.));
#12024=DIRECTION('center_axis',(0.,1.,0.));
#12025=DIRECTION('ref_axis',(1.,0.,0.));
#12026=DIRECTION('center_axis',(0.,1.,0.));
#12027=DIRECTION('ref_axis',(1.,0.,0.));
#12028=DIRECTION('',(0.,1.,0.));
#12029=DIRECTION('center_axis',(0.,-1.,0.));
#12030=DIRECTION('ref_axis',(1.,0.,0.));
#12031=DIRECTION('center_axis',(0.,1.,0.));
#12032=DIRECTION('ref_axis',(1.,0.,0.));
#12033=DIRECTION('center_axis',(0.,1.,0.));
#12034=DIRECTION('ref_axis',(1.,0.,0.));
#12035=DIRECTION('',(0.,1.,0.));
#12036=DIRECTION('center_axis',(0.,-1.,0.));
#12037=DIRECTION('ref_axis',(1.,0.,0.));
#12038=DIRECTION('center_axis',(-1.,0.,0.));
#12039=DIRECTION('ref_axis',(0.,0.,1.));
#12040=DIRECTION('',(0.,0.,-1.));
#12041=DIRECTION('',(0.,1.,0.));
#12042=DIRECTION('',(0.,0.,1.));
#12043=DIRECTION('',(0.,1.,0.));
#12044=DIRECTION('center_axis',(1.,0.,0.));
#12045=DIRECTION('ref_axis',(0.,0.,-1.));
#12046=DIRECTION('',(0.,0.,1.));
#12047=DIRECTION('',(0.,-1.,0.));
#12048=DIRECTION('',(0.,0.,-1.));
#12049=DIRECTION('',(0.,1.,0.));
#12050=DIRECTION('center_axis',(0.,0.,1.));
#12051=DIRECTION('ref_axis',(1.,0.,0.));
#12052=DIRECTION('',(-1.,0.,0.));
#12053=DIRECTION('',(1.,0.,0.));
#12054=DIRECTION('center_axis',(0.,1.,0.));
#12055=DIRECTION('ref_axis',(0.,0.,1.));
#12056=DIRECTION('',(1.,0.,0.));
#12057=DIRECTION('center_axis',(0.,1.,0.));
#12058=DIRECTION('ref_axis',(1.,0.,0.));
#12059=DIRECTION('',(-1.,0.,0.));
#12060=DIRECTION('center_axis',(-1.,0.,0.));
#12061=DIRECTION('ref_axis',(0.,0.,1.));
#12062=DIRECTION('',(0.,0.,-1.));
#12063=DIRECTION('',(0.,1.,0.));
#12064=DIRECTION('',(0.,0.,1.));
#12065=DIRECTION('',(0.,1.,0.));
#12066=DIRECTION('center_axis',(1.,0.,0.));
#12067=DIRECTION('ref_axis',(0.,0.,-1.));
#12068=DIRECTION('',(0.,0.,1.));
#12069=DIRECTION('',(0.,-1.,0.));
#12070=DIRECTION('',(0.,0.,-1.));
#12071=DIRECTION('',(0.,1.,0.));
#12072=DIRECTION('center_axis',(0.,0.,1.));
#12073=DIRECTION('ref_axis',(1.,0.,0.));
#12074=DIRECTION('',(-1.,0.,0.));
#12075=DIRECTION('',(1.,0.,0.));
#12076=DIRECTION('center_axis',(0.,1.,0.));
#12077=DIRECTION('ref_axis',(0.,0.,1.));
#12078=DIRECTION('',(1.,0.,0.));
#12079=DIRECTION('center_axis',(0.,1.,0.));
#12080=DIRECTION('ref_axis',(1.,0.,0.));
#12081=DIRECTION('',(-1.,0.,0.));
#12082=DIRECTION('center_axis',(0.,1.,0.));
#12083=DIRECTION('ref_axis',(-1.,0.,0.));
#12084=DIRECTION('',(-1.,0.,0.));
#12085=DIRECTION('',(0.,0.,1.));
#12086=DIRECTION('',(-1.,0.,0.));
#12087=DIRECTION('',(0.,0.,1.));
#12088=DIRECTION('center_axis',(1.,0.,0.));
#12089=DIRECTION('ref_axis',(0.,1.,0.));
#12090=DIRECTION('',(0.,1.,0.));
#12091=DIRECTION('',(0.,1.,0.));
#12092=DIRECTION('',(0.,0.,1.));
#12093=DIRECTION('center_axis',(0.,-1.,0.));
#12094=DIRECTION('ref_axis',(1.,0.,0.));
#12095=DIRECTION('',(1.,0.,0.));
#12096=DIRECTION('',(1.,0.,0.));
#12097=DIRECTION('',(0.,0.,1.));
#12098=DIRECTION('center_axis',(-1.,0.,0.));
#12099=DIRECTION('ref_axis',(0.,-1.,0.));
#12100=DIRECTION('',(0.,-1.,0.));
#12101=DIRECTION('',(0.,-1.,0.));
#12102=DIRECTION('center_axis',(0.,0.,1.));
#12103=DIRECTION('ref_axis',(1.,0.,0.));
#12104=DIRECTION('center_axis',(0.,0.,1.));
#12105=DIRECTION('ref_axis',(1.,0.,0.));
#14995=CARTESIAN_POINT('',(0.,0.,0.));
#14996=CARTESIAN_POINT('Origin',(1.8,13.,0.9));
#14997=CARTESIAN_POINT('',(1.525,13.,1.));
#14998=CARTESIAN_POINT('Origin',(1.8,13.,1.));
#14999=CARTESIAN_POINT('',(1.525,13.,1.4));
#15000=CARTESIAN_POINT('',(1.525,13.,0.9));
#15001=CARTESIAN_POINT('Origin',(1.8,13.,1.4));
#15002=CARTESIAN_POINT('Origin',(-1.8,17.,0.9));
#15003=CARTESIAN_POINT('',(-2.075,17.,1.));
#15004=CARTESIAN_POINT('Origin',(-1.8,17.,1.));
#15005=CARTESIAN_POINT('',(-2.075,17.,1.4));
#15006=CARTESIAN_POINT('',(-2.075,17.,0.9));
#15007=CARTESIAN_POINT('Origin',(-1.8,17.,1.4));
#15008=CARTESIAN_POINT('Origin',(-1.8,13.,0.9));
#15009=CARTESIAN_POINT('',(-2.075,13.,1.));
#15010=CARTESIAN_POINT('Origin',(-1.8,13.,1.));
#15011=CARTESIAN_POINT('',(-2.075,13.,1.4));
#15012=CARTESIAN_POINT('',(-2.075,13.,0.9));
#15013=CARTESIAN_POINT('Origin',(-1.8,13.,1.4));
#15014=CARTESIAN_POINT('Origin',(1.8,17.,0.9));
#15015=CARTESIAN_POINT('',(1.525,17.,1.));
#15016=CARTESIAN_POINT('Origin',(1.8,17.,1.));
#15017=CARTESIAN_POINT('',(1.525,17.,1.4));
#15018=CARTESIAN_POINT('',(1.525,17.,0.9));
#15019=CARTESIAN_POINT('Origin',(1.8,17.,1.4));
#15020=CARTESIAN_POINT('Origin',(0.,13.6,3.5));
#15021=CARTESIAN_POINT('',(-0.5,13.7,3.5));
#15022=CARTESIAN_POINT('Origin',(0.,13.7,3.5));
#15023=CARTESIAN_POINT('',(-0.5,14.1,3.5));
#15024=CARTESIAN_POINT('',(-0.5,13.6,3.5));
#15025=CARTESIAN_POINT('Origin',(0.,14.1,3.5));
#15026=CARTESIAN_POINT('Origin',(0.,13.6,3.5));
#15027=CARTESIAN_POINT('',(-0.5,15.9,3.5));
#15028=CARTESIAN_POINT('Origin',(0.,15.9,3.5));
#15029=CARTESIAN_POINT('',(-0.5,16.3,3.5));
#15030=CARTESIAN_POINT('',(-0.5,13.6,3.5));
#15031=CARTESIAN_POINT('Origin',(0.,16.3,3.5));
#15032=CARTESIAN_POINT('Origin',(-1.8,15.9,1.4));
#15033=CARTESIAN_POINT('',(-1.8,15.9,4.5));
#15034=CARTESIAN_POINT('',(-1.8,15.9,1.4));
#15035=CARTESIAN_POINT('',(-1.8,15.9,4.5));
#15036=CARTESIAN_POINT('',(-1.8,16.3,4.5));
#15037=CARTESIAN_POINT('',(-1.8,15.9,4.5));
#15038=CARTESIAN_POINT('',(-1.8,16.3,1.4));
#15039=CARTESIAN_POINT('',(-1.8,16.3,4.5));
#15040=CARTESIAN_POINT('',(-1.8,15.45,1.4));
#15041=CARTESIAN_POINT('Origin',(1.8,15.9,4.5));
#15042=CARTESIAN_POINT('',(1.8,15.9,1.4));
#15043=CARTESIAN_POINT('',(1.8,15.9,4.5));
#15044=CARTESIAN_POINT('',(1.8,15.9,1.4));
#15045=CARTESIAN_POINT('',(1.8,16.3,1.4));
#15046=CARTESIAN_POINT('',(1.8,15.45,1.4));
#15047=CARTESIAN_POINT('',(1.8,16.3,4.5));
#15048=CARTESIAN_POINT('',(1.8,16.3,1.4));
#15049=CARTESIAN_POINT('',(1.8,15.9,4.5));
#15050=CARTESIAN_POINT('Origin',(-1.8,15.9,4.5));
#15051=CARTESIAN_POINT('',(1.8,15.9,4.5));
#15052=CARTESIAN_POINT('',(1.8,16.3,4.5));
#15053=CARTESIAN_POINT('Origin',(0.,16.3,2.95));
#15054=CARTESIAN_POINT('',(0.,16.3,1.4));
#15055=CARTESIAN_POINT('Origin',(0.,15.9,2.95));
#15056=CARTESIAN_POINT('',(0.,15.9,1.4));
#15057=CARTESIAN_POINT('Origin',(-1.8,13.7,1.4));
#15058=CARTESIAN_POINT('',(-1.8,13.7,4.5));
#15059=CARTESIAN_POINT('',(-1.8,13.7,1.4));
#15060=CARTESIAN_POINT('',(-1.8,13.7,4.5));
#15061=CARTESIAN_POINT('',(-1.8,14.1,4.5));
#15062=CARTESIAN_POINT('',(-1.8,13.7,4.5));
#15063=CARTESIAN_POINT('',(-1.8,14.1,1.4));
#15064=CARTESIAN_POINT('',(-1.8,14.1,4.5));
#15065=CARTESIAN_POINT('',(-1.8,14.35,1.4));
#15066=CARTESIAN_POINT('Origin',(1.8,13.7,4.5));
#15067=CARTESIAN_POINT('',(1.8,13.7,1.4));
#15068=CARTESIAN_POINT('',(1.8,13.7,4.5));
#15069=CARTESIAN_POINT('',(1.8,13.7,1.4));
#15070=CARTESIAN_POINT('',(1.8,14.1,1.4));
#15071=CARTESIAN_POINT('',(1.8,14.35,1.4));
#15072=CARTESIAN_POINT('',(1.8,14.1,4.5));
#15073=CARTESIAN_POINT('',(1.8,14.1,1.4));
#15074=CARTESIAN_POINT('',(1.8,13.7,4.5));
#15075=CARTESIAN_POINT('Origin',(-1.8,13.7,4.5));
#15076=CARTESIAN_POINT('',(1.8,13.7,4.5));
#15077=CARTESIAN_POINT('',(1.8,14.1,4.5));
#15078=CARTESIAN_POINT('Origin',(0.,14.1,2.95));
#15079=CARTESIAN_POINT('',(0.,14.1,1.4));
#15080=CARTESIAN_POINT('Origin',(0.,13.7,2.95));
#15081=CARTESIAN_POINT('',(0.,13.7,1.4));
#15082=CARTESIAN_POINT('Origin',(2.5,17.5,1.));
#15083=CARTESIAN_POINT('',(2.5,17.5,1.));
#15084=CARTESIAN_POINT('',(-2.5,17.5,1.));
#15085=CARTESIAN_POINT('',(2.5,17.5,1.));
#15086=CARTESIAN_POINT('',(-2.5,17.5,1.4));
#15087=CARTESIAN_POINT('',(-2.5,17.5,1.));
#15088=CARTESIAN_POINT('',(2.5,17.5,1.4));
#15089=CARTESIAN_POINT('',(2.5,17.5,1.4));
#15090=CARTESIAN_POINT('',(2.5,17.5,1.));
#15091=CARTESIAN_POINT('Origin',(2.5,12.5,1.));
#15092=CARTESIAN_POINT('',(2.5,12.5,1.));
#15093=CARTESIAN_POINT('',(2.5,12.5,1.));
#15094=CARTESIAN_POINT('',(2.5,12.5,1.4));
#15095=CARTESIAN_POINT('',(2.5,12.5,1.4));
#15096=CARTESIAN_POINT('',(2.5,12.5,1.));
#15097=CARTESIAN_POINT('Origin',(-2.5,12.5,1.));
#15098=CARTESIAN_POINT('',(-2.5,12.5,1.));
#15099=CARTESIAN_POINT('',(-2.5,12.5,1.));
#15100=CARTESIAN_POINT('',(-2.5,12.5,1.4));
#15101=CARTESIAN_POINT('',(-2.5,12.5,1.4));
#15102=CARTESIAN_POINT('',(-2.5,12.5,1.));
#15103=CARTESIAN_POINT('Origin',(-2.5,17.5,1.));
#15104=CARTESIAN_POINT('',(-2.5,17.5,1.));
#15105=CARTESIAN_POINT('',(-2.5,17.5,1.4));
#15106=CARTESIAN_POINT('Origin',(0.,15.,1.4));
#15107=CARTESIAN_POINT('Origin',(0.,15.,1.));
#16183=UNCERTAINTY_MEASURE_WITH_UNIT(LENGTH_MEASURE(0.001),#16282,
'DISTANCE_ACCURACY_VALUE',
'Maximum model space distance between geometric entities at asserted c
onnectivities');
#16212=UNCERTAINTY_MEASURE_WITH_UNIT(LENGTH_MEASURE(0.001),#16282,
'DISTANCE_ACCURACY_VALUE',
'Maximum model space distance between geometric entities at asserted c
onnectivities');
#16252=(
GEOMETRIC_REPRESENTATION_CONTEXT(3)
GLOBAL_UNCERTAINTY_ASSIGNED_CONTEXT((#16183))
GLOBAL_UNIT_ASSIGNED_CONTEXT((#16282,#16284,#16285))
REPRESENTATION_CONTEXT('','3D')
);
#16281=(
GEOMETRIC_REPRESENTATION_CONTEXT(3)
GLOBAL_UNCERTAINTY_ASSIGNED_CONTEXT((#16212))
GLOBAL_UNIT_ASSIGNED_CONTEXT((#16282,#16284,#16285))
REPRESENTATION_CONTEXT('','3D')
);
#16282=(
LENGTH_UNIT()
NAMED_UNIT(*)
SI_UNIT(.CENTI.,.METRE.)
);
#16284=(
NAMED_UNIT(*)
PLANE_ANGLE_UNIT()
SI_UNIT($,.RADIAN.)
);
#16285=(
NAMED_UNIT(*)
SI_UNIT($,.STERADIAN.)
SOLID_ANGLE_UNIT()
);
#16325=SHAPE_DEFINITION_REPRESENTATION(#16419,#16558);
#16419=PRODUCT_DEFINITION_SHAPE('',$,#16627);
#16558=SHAPE_REPRESENTATION('',(#9764),#16252);
#16587=PRODUCT_DEFINITION_CONTEXT('part definition',#16793,'design');
#16627=PRODUCT_DEFINITION('Roller bracket (3)','Roller bracket (3)',#16695,
#16587);
#16695=PRODUCT_DEFINITION_FORMATION('',$,#16834);
#16793=APPLICATION_CONTEXT(
'Core Data for Automotive Mechanical Design Process');
#16794=PRODUCT_CONTEXT('part definition',#16793,'mechanical');
#16834=PRODUCT('Roller bracket (3)','Roller bracket (3)','Roller bracket (3)',
(#16794));
#16905=COLOUR_RGB('Dark Blue',0.08,0.2,0.34);
#16906=FILL_AREA_STYLE_COLOUR('',#16905);
#16907=FILL_AREA_STYLE('',(#16906));
#16908=SURFACE_STYLE_FILL_AREA(#16907);
#16909=SURFACE_SIDE_STYLE('',(#16908));
#16910=SURFACE_STYLE_USAGE(.BOTH.,#16909);
#16911=PRESENTATION_STYLE_ASSIGNMENT((#16910));
ENDSEC;
END-ISO-10303-21;
